ISO-10303-21;
HEADER;
/* Generated by software containing ST-Developer
 * from STEP Tools, Inc. (www.steptools.com) 
 */

FILE_DESCRIPTION(
/* description */ ('Belt-driven linear axis on 2020 extrusion'),
/* implementation_level */ '2;1');

FILE_NAME(
/* name */ 'Input M3 set screw.step',
/* time_stamp */ '2026-10-28T03:26:09-07:00',
/* author */ (''),
/* organization */ (''),
/* preprocessor_version */ 'ST-DEVELOPER v20.2',
/* originating_system */ 'Autodesk Translation Framework v15.17.0.0',
/* authorisation */ '');

FILE_SCHEMA (('AUTOMOTIVE_DESIGN { 1 0 10303 214 3 1 1 }'));
ENDSEC;

DATA;
#10=MECHANICAL_DESIGN_GEOMETRIC_PRESENTATION_REPRESENTATION('',(#646),#20096);
#544=SHAPE_REPRESENTATION_RELATIONSHIP('SRR','None',#20342,#590);
#590=ADVANCED_BREP_SHAPE_REPRESENTATION('',(#701),#20073);
#646=STYLED_ITEM('',(#20657),#701);
#701=MANIFOLD_SOLID_BREP('Body1',#10960);
#1121=PLANE('',#12237);
#1122=PLANE('',#12238);
#1639=FACE_OUTER_BOUND('',#2381,.T.);
#1640=FACE_OUTER_BOUND('',#2382,.T.);
#1641=FACE_OUTER_BOUND('',#2383,.T.);
#2381=EDGE_LOOP('',(#9025,#9026,#9027,#9028));
#2382=EDGE_LOOP('',(#9029));
#2383=EDGE_LOOP('',(#9030));
#3214=LINE('',#18484,#4071);
#4071=VECTOR('',#14826,0.15);
#4696=CIRCLE('',#12235,0.15);
#4697=CIRCLE('',#12236,0.15);
#5491=VERTEX_POINT('',#18481);
#5492=VERTEX_POINT('',#18483);
#6727=EDGE_CURVE('',#5491,#5491,#4696,.T.);
#6728=EDGE_CURVE('',#5491,#5492,#3214,.T.);
#6729=EDGE_CURVE('',#5492,#5492,#4697,.T.);
#9025=ORIENTED_EDGE('',*,*,#6727,.F.);
#9026=ORIENTED_EDGE('',*,*,#6728,.T.);
#9027=ORIENTED_EDGE('',*,*,#6729,.T.);
#9028=ORIENTED_EDGE('',*,*,#6728,.F.);
#9029=ORIENTED_EDGE('',*,*,#6727,.T.);
#9030=ORIENTED_EDGE('',*,*,#6729,.F.);
#10209=CYLINDRICAL_SURFACE('',#12234,0.15);
#10690=ADVANCED_FACE('',(#1639),#10209,.T.);
#10691=ADVANCED_FACE('',(#1640),#1121,.T.);
#10692=ADVANCED_FACE('',(#1641),#1122,.F.);
#10960=CLOSED_SHELL('',(#10690,#10691,#10692));
#12233=AXIS2_PLACEMENT_3D('',#18479,#14820,#14821);
#12234=AXIS2_PLACEMENT_3D('',#18480,#14822,#14823);
#12235=AXIS2_PLACEMENT_3D('',#18482,#14824,#14825);
#12236=AXIS2_PLACEMENT_3D('',#18485,#14827,#14828);
#12237=AXIS2_PLACEMENT_3D('',#18486,#14829,#14830);
#12238=AXIS2_PLACEMENT_3D('',#18487,#14831,#14832);
#14820=DIRECTION('axis',(0.,0.,1.));
#14821=DIRECTION('refdir',(1.,0.,0.));
#14822=DIRECTION('center_axis',(0.,0.,1.));
#14823=DIRECTION('ref_axis',(1.,0.,0.));
#14824=DIRECTION('center_axis',(0.,0.,1.));
#14825=DIRECTION('ref_axis',(1.,0.,0.));
#14826=DIRECTION('',(0.,0.,-1.));
#14827=DIRECTION('center_axis',(0.,0.,1.));
#14828=DIRECTION('ref_axis',(1.,0.,0.));
#14829=DIRECTION('center_axis',(0.,0.,1.));
#14830=DIRECTION('ref_axis',(1.,0.,0.));
#14831=DIRECTION('center_axis',(0.,0.,1.));
#14832=DIRECTION('ref_axis',(1.,0.,0.));
#18479=CARTESIAN_POINT('',(0.,0.,0.));
#18480=CARTESIAN_POINT('Origin',(0.,-3.95,6.35));
#18481=CARTESIAN_POINT('',(-0.15,-3.95,6.6));
#18482=CARTESIAN_POINT('Origin',(0.,-3.95,6.6));
#18483=CARTESIAN_POINT('',(-0.15,-3.95,6.35));
#18484=CARTESIAN_POINT('',(-0.15,-3.95,6.35));
#18485=CARTESIAN_POINT('Origin',(0.,-3.95,6.35));
#18486=CARTESIAN_POINT('Origin',(0.,-3.95,6.6));
#18487=CARTESIAN_POINT('Origin',(0.,-3.95,6.35));
#20019=UNCERTAINTY_MEASURE_WITH_UNIT(LENGTH_MEASURE(0.001),#20097,
'DISTANCE_ACCURACY_VALUE',
'Maximum model space distance between geometric entities at asserted c
onnectivities');
#20042=UNCERTAINTY_MEASURE_WITH_UNIT(LENGTH_MEASURE(0.001),#20097,
'DISTANCE_ACCURACY_VALUE',
'Maximum model space distance between geometric entities at asserted c
onnectivities');
#20073=(
GEOMETRIC_REPRESENTATION_CONTEXT(3)
GLOBAL_UNCERTAINTY_ASSIGNED_CONTEXT((#20019))
GLOBAL_UNIT_ASSIGNED_CONTEXT((#20097,#20099,#20100))
REPRESENTATION_CONTEXT('','3D')
);
#20096=(
GEOMETRIC_REPRESENTATION_CONTEXT(3)
GLOBAL_UNCERTAINTY_ASSIGNED_CONTEXT((#20042))
GLOBAL_UNIT_ASSIGNED_CONTEXT((#20097,#20099,#20100))
REPRESENTATION_CONTEXT('','3D')
);
#20097=(
LENGTH_UNIT()
NAMED_UNIT(*)
SI_UNIT(.CENTI.,.METRE.)
);
#20099=(
NAMED_UNIT(*)
PLANE_ANGLE_UNIT()
SI_UNIT($,.RADIAN.)
);
#20100=(
NAMED_UNIT(*)
SI_UNIT($,.STERADIAN.)
SOLID_ANGLE_UNIT()
);
#20131=SHAPE_DEFINITION_REPRESENTATION(#20189,#20342);
#20189=PRODUCT_DEFINITION_SHAPE('',$,#20396);
#20342=SHAPE_REPRESENTATION('',(#12233),#20073);
#20365=PRODUCT_DEFINITION_CONTEXT('part definition',#20526,'design');
#20396=PRODUCT_DEFINITION('Input M3 set screw','Input M3 set screw',#20449,
#20365);
#20449=PRODUCT_DEFINITION_FORMATION('',$,#20558);
#20526=APPLICATION_CONTEXT(
'Core Data for Automotive Mechanical Design Process');
#20527=PRODUCT_CONTEXT('part definition',#20526,'mechanical');
#20558=PRODUCT('Input M3 set screw','Input M3 set screw',
'Input M3 set screw',(#20527));
#20651=COLOUR_RGB('Black',0.12,0.14,0.17);
#20652=FILL_AREA_STYLE_COLOUR('',#20651);
#20653=FILL_AREA_STYLE('',(#20652));
#20654=SURFACE_STYLE_FILL_AREA(#20653);
#20655=SURFACE_SIDE_STYLE('',(#20654));
#20656=SURFACE_STYLE_USAGE(.BOTH.,#20655);
#20657=PRESENTATION_STYLE_ASSIGNMENT((#20656));
ENDSEC;
END-ISO-10303-21;
